ISO-10303-21;
HEADER;
/* Generated by software containing ST-Developer
 * from STEP Tools, Inc. (www.steptools.com) 
 */

FILE_DESCRIPTION(
/* description */ ('STEP AP214'),
/* implementation_level */ '2;1');

FILE_NAME(
/* name */ 'PRT-TQ-1012-05.step',
/* time_stamp */ '2026-10-07T12:49:37-07:00',
/* author */ (''),
/* organization */ (''),
/* preprocessor_version */ 'ST-DEVELOPER v20.2',
/* originating_system */ 'Autodesk Translation Framework v15.15.0.0',
/* authorisation */ '');

FILE_SCHEMA (('AUTOMOTIVE_DESIGN { 1 0 10303 214 3 1 1 }'));
ENDSEC;

DATA;
#10=MECHANICAL_DESIGN_GEOMETRIC_PRESENTATION_REPRESENTATION('',(#315),#33016);
#257=SHAPE_REPRESENTATION_RELATIONSHIP('SRR','None',#33152,#284);
#284=ADVANCED_BREP_SHAPE_REPRESENTATION('',(#342),#33013);
#315=STYLED_ITEM('',(#33284),#342);
#342=MANIFOLD_SOLID_BREP('Body1',#9966);
#368=CONICAL_SURFACE('',#11162,11.,1.36330010035969);
#369=CONICAL_SURFACE('',#11173,15.25,0.785398163397438);
#370=CONICAL_SURFACE('',#11174,12.3985,0.785398163397449);
#371=CONICAL_SURFACE('',#11180,9.,0.785398163397453);
#550=FACE_BOUND('',#2179,.T.);
#551=FACE_BOUND('',#2187,.T.);
#1008=PLANE('',#11160);
#1009=PLANE('',#11167);
#1010=PLANE('',#11176);
#1011=PLANE('',#11182);
#1543=FACE_OUTER_BOUND('',#2175,.T.);
#1544=FACE_OUTER_BOUND('',#2176,.T.);
#1545=FACE_OUTER_BOUND('',#2177,.T.);
#1546=FACE_OUTER_BOUND('',#2178,.T.);
#1547=FACE_OUTER_BOUND('',#2180,.T.);
#1548=FACE_OUTER_BOUND('',#2181,.T.);
#1549=FACE_OUTER_BOUND('',#2182,.T.);
#1550=FACE_OUTER_BOUND('',#2183,.T.);
#1551=FACE_OUTER_BOUND('',#2184,.T.);
#1552=FACE_OUTER_BOUND('',#2185,.T.);
#1553=FACE_OUTER_BOUND('',#2186,.T.);
#2175=EDGE_LOOP('',(#9066));
#2176=EDGE_LOOP('',(#9067,#9068,#9069,#9070));
#2177=EDGE_LOOP('',(#9071,#9072,#9073,#9074,#9075));
#2178=EDGE_LOOP('',(#9076));
#2179=EDGE_LOOP('',(#9077));
#2180=EDGE_LOOP('',(#9078,#9079,#9080,#9081,#9082));
#2181=EDGE_LOOP('',(#9083,#9084,#9085,#9086,#9087));
#2182=EDGE_LOOP('',(#9088,#9089,#9090,#9091,#9092));
#2183=EDGE_LOOP('',(#9093));
#2184=EDGE_LOOP('',(#9094,#9095,#9096,#9097));
#2185=EDGE_LOOP('',(#9098,#9099,#9100,#9101));
#2186=EDGE_LOOP('',(#9102));
#2187=EDGE_LOOP('',(#9103));
#2572=CIRCLE('',#11161,11.);
#2573=CIRCLE('',#11163,15.75);
#2574=CIRCLE('',#11165,15.75);
#2575=CIRCLE('',#11166,15.75);
#2576=CIRCLE('',#11168,15.25);
#2577=CIRCLE('',#11169,13.5);
#2578=CIRCLE('',#11171,13.5);
#2579=CIRCLE('',#11172,13.5);
#2580=CIRCLE('',#11175,12.3985);
#2581=CIRCLE('',#11177,9.);
#2582=CIRCLE('',#11179,9.);
#2583=CIRCLE('',#11181,10.);
#3324=LINE('',#32737,#4074);
#3325=LINE('',#32743,#4075);
#3326=LINE('',#32754,#4076);
#3327=LINE('',#32756,#4077);
#3328=LINE('',#32759,#4078);
#3329=LINE('',#32766,#4079);
#3330=LINE('',#32770,#4080);
#4074=VECTOR('',#13751,11.);
#4075=VECTOR('',#13758,15.75);
#4076=VECTOR('',#13771,13.5);
#4077=VECTOR('',#13774,15.25);
#4078=VECTOR('',#13777,12.3985);
#4079=VECTOR('',#13786,9.);
#4080=VECTOR('',#13791,9.);
#4974=VERTEX_POINT('',#32732);
#4975=VERTEX_POINT('',#32735);
#4976=VERTEX_POINT('',#32739);
#4977=VERTEX_POINT('',#32740);
#4978=VERTEX_POINT('',#32745);
#4979=VERTEX_POINT('',#32747);
#4980=VERTEX_POINT('',#32750);
#4981=VERTEX_POINT('',#32751);
#4982=VERTEX_POINT('',#32758);
#4983=VERTEX_POINT('',#32762);
#4984=VERTEX_POINT('',#32765);
#4985=VERTEX_POINT('',#32769);
#6346=EDGE_CURVE('',#4974,#4974,#2572,.T.);
#6347=EDGE_CURVE('',#4975,#4975,#2573,.T.);
#6348=EDGE_CURVE('',#4975,#4974,#3324,.T.);
#6349=EDGE_CURVE('',#4976,#4977,#2574,.T.);
#6350=EDGE_CURVE('',#4977,#4976,#2575,.T.);
#6351=EDGE_CURVE('',#4976,#4975,#3325,.T.);
#6352=EDGE_CURVE('',#4978,#4978,#2576,.T.);
#6353=EDGE_CURVE('',#4979,#4979,#2577,.T.);
#6354=EDGE_CURVE('',#4980,#4981,#2578,.T.);
#6355=EDGE_CURVE('',#4981,#4980,#2579,.T.);
#6356=EDGE_CURVE('',#4980,#4979,#3326,.T.);
#6357=EDGE_CURVE('',#4977,#4978,#3327,.T.);
#6358=EDGE_CURVE('',#4981,#4982,#3328,.T.);
#6359=EDGE_CURVE('',#4982,#4982,#2580,.T.);
#6360=EDGE_CURVE('',#4983,#4983,#2581,.T.);
#6361=EDGE_CURVE('',#4983,#4984,#3329,.T.);
#6362=EDGE_CURVE('',#4984,#4984,#2582,.T.);
#6363=EDGE_CURVE('',#4984,#4985,#3330,.T.);
#6364=EDGE_CURVE('',#4985,#4985,#2583,.T.);
#9066=ORIENTED_EDGE('',*,*,#6346,.F.);
#9067=ORIENTED_EDGE('',*,*,#6347,.F.);
#9068=ORIENTED_EDGE('',*,*,#6348,.T.);
#9069=ORIENTED_EDGE('',*,*,#6346,.T.);
#9070=ORIENTED_EDGE('',*,*,#6348,.F.);
#9071=ORIENTED_EDGE('',*,*,#6349,.T.);
#9072=ORIENTED_EDGE('',*,*,#6350,.T.);
#9073=ORIENTED_EDGE('',*,*,#6351,.T.);
#9074=ORIENTED_EDGE('',*,*,#6347,.T.);
#9075=ORIENTED_EDGE('',*,*,#6351,.F.);
#9076=ORIENTED_EDGE('',*,*,#6352,.T.);
#9077=ORIENTED_EDGE('',*,*,#6353,.F.);
#9078=ORIENTED_EDGE('',*,*,#6354,.T.);
#9079=ORIENTED_EDGE('',*,*,#6355,.T.);
#9080=ORIENTED_EDGE('',*,*,#6356,.T.);
#9081=ORIENTED_EDGE('',*,*,#6353,.T.);
#9082=ORIENTED_EDGE('',*,*,#6356,.F.);
#9083=ORIENTED_EDGE('',*,*,#6349,.F.);
#9084=ORIENTED_EDGE('',*,*,#6350,.F.);
#9085=ORIENTED_EDGE('',*,*,#6357,.T.);
#9086=ORIENTED_EDGE('',*,*,#6352,.F.);
#9087=ORIENTED_EDGE('',*,*,#6357,.F.);
#9088=ORIENTED_EDGE('',*,*,#6354,.F.);
#9089=ORIENTED_EDGE('',*,*,#6355,.F.);
#9090=ORIENTED_EDGE('',*,*,#6358,.T.);
#9091=ORIENTED_EDGE('',*,*,#6359,.T.);
#9092=ORIENTED_EDGE('',*,*,#6358,.F.);
#9093=ORIENTED_EDGE('',*,*,#6360,.T.);
#9094=ORIENTED_EDGE('',*,*,#6360,.F.);
#9095=ORIENTED_EDGE('',*,*,#6361,.T.);
#9096=ORIENTED_EDGE('',*,*,#6362,.T.);
#9097=ORIENTED_EDGE('',*,*,#6361,.F.);
#9098=ORIENTED_EDGE('',*,*,#6362,.F.);
#9099=ORIENTED_EDGE('',*,*,#6363,.T.);
#9100=ORIENTED_EDGE('',*,*,#6364,.F.);
#9101=ORIENTED_EDGE('',*,*,#6363,.F.);
#9102=ORIENTED_EDGE('',*,*,#6359,.F.);
#9103=ORIENTED_EDGE('',*,*,#6364,.T.);
#9382=CYLINDRICAL_SURFACE('',#11164,15.75);
#9383=CYLINDRICAL_SURFACE('',#11170,13.5);
#9384=CYLINDRICAL_SURFACE('',#11178,9.);
#9909=ADVANCED_FACE('',(#1543),#1008,.F.);
#9910=ADVANCED_FACE('',(#1544),#368,.T.);
#9911=ADVANCED_FACE('',(#1545),#9382,.T.);
#9912=ADVANCED_FACE('',(#1546,#550),#1009,.F.);
#9913=ADVANCED_FACE('',(#1547),#9383,.T.);
#9914=ADVANCED_FACE('',(#1548),#369,.T.);
#9915=ADVANCED_FACE('',(#1549),#370,.T.);
#9916=ADVANCED_FACE('',(#1550),#1010,.T.);
#9917=ADVANCED_FACE('',(#1551),#9384,.F.);
#9918=ADVANCED_FACE('',(#1552),#371,.F.);
#9919=ADVANCED_FACE('',(#1553,#551),#1011,.F.);
#9966=CLOSED_SHELL('',(#9909,#9910,#9911,#9912,#9913,#9914,#9915,#9916,
#9917,#9918,#9919));
#11159=AXIS2_PLACEMENT_3D('',#32730,#13741,#13742);
#11160=AXIS2_PLACEMENT_3D('',#32731,#13743,#13744);
#11161=AXIS2_PLACEMENT_3D('',#32733,#13745,#13746);
#11162=AXIS2_PLACEMENT_3D('',#32734,#13747,#13748);
#11163=AXIS2_PLACEMENT_3D('',#32736,#13749,#13750);
#11164=AXIS2_PLACEMENT_3D('',#32738,#13752,#13753);
#11165=AXIS2_PLACEMENT_3D('',#32741,#13754,#13755);
#11166=AXIS2_PLACEMENT_3D('',#32742,#13756,#13757);
#11167=AXIS2_PLACEMENT_3D('',#32744,#13759,#13760);
#11168=AXIS2_PLACEMENT_3D('',#32746,#13761,#13762);
#11169=AXIS2_PLACEMENT_3D('',#32748,#13763,#13764);
#11170=AXIS2_PLACEMENT_3D('',#32749,#13765,#13766);
#11171=AXIS2_PLACEMENT_3D('',#32752,#13767,#13768);
#11172=AXIS2_PLACEMENT_3D('',#32753,#13769,#13770);
#11173=AXIS2_PLACEMENT_3D('',#32755,#13772,#13773);
#11174=AXIS2_PLACEMENT_3D('',#32757,#13775,#13776);
#11175=AXIS2_PLACEMENT_3D('',#32760,#13778,#13779);
#11176=AXIS2_PLACEMENT_3D('',#32761,#13780,#13781);
#11177=AXIS2_PLACEMENT_3D('',#32763,#13782,#13783);
#11178=AXIS2_PLACEMENT_3D('',#32764,#13784,#13785);
#11179=AXIS2_PLACEMENT_3D('',#32767,#13787,#13788);
#11180=AXIS2_PLACEMENT_3D('',#32768,#13789,#13790);
#11181=AXIS2_PLACEMENT_3D('',#32771,#13792,#13793);
#11182=AXIS2_PLACEMENT_3D('',#32772,#13794,#13795);
#13741=DIRECTION('axis',(0.,0.,1.));
#13742=DIRECTION('refdir',(1.,0.,0.));
#13743=DIRECTION('center_axis',(0.,-1.,0.));
#13744=DIRECTION('ref_axis',(0.,0.,-1.));
#13745=DIRECTION('center_axis',(0.,-1.,0.));
#13746=DIRECTION('ref_axis',(0.,0.,-1.));
#13747=DIRECTION('center_axis',(0.,-1.,0.));
#13748=DIRECTION('ref_axis',(0.,0.,-1.));
#13749=DIRECTION('center_axis',(0.,-1.,0.));
#13750=DIRECTION('ref_axis',(0.,0.,-1.));
#13751=DIRECTION('',(1.19837786199035E-16,0.206010481049842,-0.978549784986749));
#13752=DIRECTION('center_axis',(0.,-1.,0.));
#13753=DIRECTION('ref_axis',(0.,0.,-1.));
#13754=DIRECTION('center_axis',(0.,1.,0.));
#13755=DIRECTION('ref_axis',(0.,0.,1.));
#13756=DIRECTION('center_axis',(0.,1.,0.));
#13757=DIRECTION('ref_axis',(0.,0.,1.));
#13758=DIRECTION('',(0.,1.,0.));
#13759=DIRECTION('center_axis',(0.,1.,0.));
#13760=DIRECTION('ref_axis',(0.,0.,1.));
#13761=DIRECTION('center_axis',(0.,-1.,0.));
#13762=DIRECTION('ref_axis',(0.,0.,1.));
#13763=DIRECTION('center_axis',(0.,-1.,0.));
#13764=DIRECTION('ref_axis',(0.,0.,-1.));
#13765=DIRECTION('center_axis',(0.,-1.,0.));
#13766=DIRECTION('ref_axis',(0.,0.,-1.));
#13767=DIRECTION('center_axis',(0.,1.,0.));
#13768=DIRECTION('ref_axis',(0.,0.,1.));
#13769=DIRECTION('center_axis',(0.,1.,0.));
#13770=DIRECTION('ref_axis',(0.,0.,1.));
#13771=DIRECTION('',(0.,1.,0.));
#13772=DIRECTION('center_axis',(0.,1.,0.));
#13773=DIRECTION('ref_axis',(0.,0.,1.));
#13774=DIRECTION('',(8.65956056235484E-17,-0.707106781186555,0.70710678118654));
#13775=DIRECTION('center_axis',(0.,1.,0.));
#13776=DIRECTION('ref_axis',(0.,0.,1.));
#13777=DIRECTION('',(8.65956056235494E-17,-0.707106781186547,0.707106781186548));
#13778=DIRECTION('center_axis',(0.,1.,0.));
#13779=DIRECTION('ref_axis',(0.,0.,1.));
#13780=DIRECTION('center_axis',(0.,-1.,0.));
#13781=DIRECTION('ref_axis',(0.,0.,-1.));
#13782=DIRECTION('center_axis',(0.,-1.,0.));
#13783=DIRECTION('ref_axis',(0.,0.,-1.));
#13784=DIRECTION('center_axis',(0.,-1.,0.));
#13785=DIRECTION('ref_axis',(0.,0.,-1.));
#13786=DIRECTION('',(0.,-1.,0.));
#13787=DIRECTION('center_axis',(0.,-1.,0.));
#13788=DIRECTION('ref_axis',(0.,0.,1.));
#13789=DIRECTION('center_axis',(0.,-1.,0.));
#13790=DIRECTION('ref_axis',(0.,0.,-1.));
#13791=DIRECTION('',(-8.65956056235497E-17,-0.707106781186545,0.707106781186551));
#13792=DIRECTION('center_axis',(0.,1.,0.));
#13793=DIRECTION('ref_axis',(0.,0.,1.));
#13794=DIRECTION('center_axis',(0.,1.,0.));
#13795=DIRECTION('ref_axis',(0.,0.,1.));
#32730=CARTESIAN_POINT('',(0.,0.,0.));
#32731=CARTESIAN_POINT('Origin',(0.,15.5,0.));
#32732=CARTESIAN_POINT('',(-1.34711147906209E-15,15.5,11.));
#32733=CARTESIAN_POINT('Origin',(0.,15.5,0.));
#32734=CARTESIAN_POINT('Origin',(0.,15.5,0.));
#32735=CARTESIAN_POINT('',(-1.92881870865708E-15,14.5,15.75));
#32736=CARTESIAN_POINT('Origin',(0.,14.5,0.));
#32737=CARTESIAN_POINT('',(-1.34711147906209E-15,15.5,11.));
#32738=CARTESIAN_POINT('Origin',(0.,0.,0.));
#32739=CARTESIAN_POINT('',(0.,9.00000000000002,15.75));
#32740=CARTESIAN_POINT('',(-1.92881870865708E-15,9.00000000000002,-15.75));
#32741=CARTESIAN_POINT('Origin',(0.,9.00000000000002,0.));
#32742=CARTESIAN_POINT('Origin',(0.,9.00000000000002,0.));
#32743=CARTESIAN_POINT('',(-1.92881870865708E-15,0.,15.75));
#32744=CARTESIAN_POINT('Origin',(-14.25,8.5,0.));
#32745=CARTESIAN_POINT('',(-1.86758636869971E-15,8.5,-15.25));
#32746=CARTESIAN_POINT('Origin',(0.,8.5,0.));
#32747=CARTESIAN_POINT('',(-1.65327317884893E-15,8.5,13.5));
#32748=CARTESIAN_POINT('Origin',(0.,8.5,0.));
#32749=CARTESIAN_POINT('Origin',(0.,0.,0.));
#32750=CARTESIAN_POINT('',(0.,1.1015,13.5));
#32751=CARTESIAN_POINT('',(-1.65327317884893E-15,1.1015,-13.5));
#32752=CARTESIAN_POINT('Origin',(0.,1.1015,0.));
#32753=CARTESIAN_POINT('Origin',(0.,1.1015,0.));
#32754=CARTESIAN_POINT('',(-1.65327317884893E-15,0.,13.5));
#32755=CARTESIAN_POINT('Origin',(0.,8.5,0.));
#32756=CARTESIAN_POINT('',(-1.86758636869971E-15,8.5,-15.25));
#32757=CARTESIAN_POINT('Origin',(0.,0.,0.));
#32758=CARTESIAN_POINT('',(-1.51837833392285E-15,-2.7393655125078E-16,-12.3985));
#32759=CARTESIAN_POINT('',(-1.51837833392285E-15,0.,-12.3985));
#32760=CARTESIAN_POINT('Origin',(0.,0.,0.));
#32761=CARTESIAN_POINT('Origin',(0.,10.,0.));
#32762=CARTESIAN_POINT('',(-1.10218211923262E-15,10.,9.));
#32763=CARTESIAN_POINT('Origin',(0.,10.,0.));
#32764=CARTESIAN_POINT('Origin',(0.,10.,0.));
#32765=CARTESIAN_POINT('',(0.,1.00000000000001,9.));
#32766=CARTESIAN_POINT('',(-1.10218211923262E-15,10.,9.));
#32767=CARTESIAN_POINT('Origin',(0.,1.00000000000001,0.));
#32768=CARTESIAN_POINT('Origin',(0.,1.00000000000001,0.));
#32769=CARTESIAN_POINT('',(0.,-8.72560844392489E-16,10.));
#32770=CARTESIAN_POINT('',(-1.10218211923262E-15,1.00000000000001,9.));
#32771=CARTESIAN_POINT('Origin',(0.,-8.72560844392489E-16,0.));
#32772=CARTESIAN_POINT('Origin',(0.,-8.72560844392489E-16,0.));
#32981=UNCERTAINTY_MEASURE_WITH_UNIT(LENGTH_MEASURE(0.01),#33017,
'DISTANCE_ACCURACY_VALUE',
'Maximum model space distance between geometric entities at asserted c
onnectivities');
#32984=UNCERTAINTY_MEASURE_WITH_UNIT(LENGTH_MEASURE(0.01),#33017,
'DISTANCE_ACCURACY_VALUE',
'Maximum model space distance between geometric entities at asserted c
onnectivities');
#33013=(
GEOMETRIC_REPRESENTATION_CONTEXT(3)
GLOBAL_UNCERTAINTY_ASSIGNED_CONTEXT((#32981))
GLOBAL_UNIT_ASSIGNED_CONTEXT((#33017,#33019,#33020))
REPRESENTATION_CONTEXT('','3D')
);
#33016=(
GEOMETRIC_REPRESENTATION_CONTEXT(3)
GLOBAL_UNCERTAINTY_ASSIGNED_CONTEXT((#32984))
GLOBAL_UNIT_ASSIGNED_CONTEXT((#33017,#33019,#33020))
REPRESENTATION_CONTEXT('','3D')
);
#33017=(
LENGTH_UNIT()
NAMED_UNIT(*)
SI_UNIT(.MILLI.,.METRE.)
);
#33019=(
NAMED_UNIT(*)
PLANE_ANGLE_UNIT()
SI_UNIT($,.RADIAN.)
);
#33020=(
NAMED_UNIT(*)
SI_UNIT($,.STERADIAN.)
SOLID_ANGLE_UNIT()
);
#33049=SHAPE_DEFINITION_REPRESENTATION(#33111,#33152);
#33111=PRODUCT_DEFINITION_SHAPE('',$,#33184);
#33152=SHAPE_REPRESENTATION('',(#11159),#33013);
#33155=PRODUCT_DEFINITION_CONTEXT('part definition',#33250,'design');
#33184=PRODUCT_DEFINITION(
'P_Torque Wrench_End Cap_PRT-TQ-1012-05_M_Rev00','PRT-TQ-1012-05',#33215,
#33155);
#33215=PRODUCT_DEFINITION_FORMATION('',$,#33280);
#33250=APPLICATION_CONTEXT(
'Core Data for Automotive Mechanical Design Process');
#33251=PRODUCT_CONTEXT('part definition',#33250,'mechanical');
#33280=PRODUCT('P_Torque Wrench_End Cap_PRT-TQ-1012-05_M_Rev00',
'PRT-TQ-1012-05',$,(#33251));
#33284=PRESENTATION_STYLE_ASSIGNMENT((#33291));
#33291=SURFACE_STYLE_USAGE(.BOTH.,#33298);
#33298=SURFACE_SIDE_STYLE('',(#33305));
#33305=SURFACE_STYLE_FILL_AREA(#33312);
#33312=FILL_AREA_STYLE('Opaque(186,91,6)',(#33319));
#33319=FILL_AREA_STYLE_COLOUR('Opaque(186,91,6)',#33326);
#33326=COLOUR_RGB('Opaque(186,91,6)', 0.09019608, 0.27058824, 0.51372549);
ENDSEC;
END-ISO-10303-21;
